ISO-10303-21;
HEADER;
/* Generated by software containing ST-Developer
 * from STEP Tools, Inc. (www.steptools.com) 
 */

FILE_DESCRIPTION(
/* description */ ('Hand wheel with handle and shaft collar'),
/* implementation_level */ '2;1');

FILE_NAME(
/* name */ 'Cap Screw - M4x16.step',
/* time_stamp */ '2026-10-28T03:23:19-07:00',
/* author */ (''),
/* organization */ (''),
/* preprocessor_version */ 'ST-DEVELOPER v20.2',
/* originating_system */ 'Autodesk Translation Framework v15.17.0.0',
/* authorisation */ '');

FILE_SCHEMA (('AUTOMOTIVE_DESIGN { 1 0 10303 214 3 1 1 }'));
ENDSEC;

DATA;
#10=MECHANICAL_DESIGN_GEOMETRIC_PRESENTATION_REPRESENTATION('',(#439),#10510);
#321=CONICAL_SURFACE('',#6329,0.325,0.785398163397448);
#322=CONICAL_SURFACE('',#6333,0.335,0.785398163397448);
#323=CONICAL_SURFACE('',#6337,0.21,0.463647609000806);
#324=CONICAL_SURFACE('',#6341,0.18,0.785398163397448);
#327=ORIENTED_CLOSED_SHELL('',*,#5341,.F.);
#330=BREP_WITH_VOIDS('Body1',#5340,(#327));
#360=SHAPE_REPRESENTATION_RELATIONSHIP('SRR','None',#10679,#392);
#392=ADVANCED_BREP_SHAPE_REPRESENTATION('',(#330),#10506);
#439=STYLED_ITEM('',(#10915),#330);
#592=FACE_BOUND('',#1485,.T.);
#747=PLANE('',#6327);
#748=PLANE('',#6335);
#749=PLANE('',#6343);
#750=PLANE('',#6344);
#751=PLANE('',#6345);
#752=PLANE('',#6346);
#753=PLANE('',#6347);
#754=PLANE('',#6348);
#755=PLANE('',#6349);
#756=PLANE('',#6350);
#757=PLANE('',#6351);
#1055=FACE_OUTER_BOUND('',#1480,.T.);
#1056=FACE_OUTER_BOUND('',#1481,.T.);
#1057=FACE_OUTER_BOUND('',#1482,.T.);
#1058=FACE_OUTER_BOUND('',#1483,.T.);
#1059=FACE_OUTER_BOUND('',#1484,.T.);
#1060=FACE_OUTER_BOUND('',#1486,.T.);
#1061=FACE_OUTER_BOUND('',#1487,.T.);
#1062=FACE_OUTER_BOUND('',#1488,.T.);
#1063=FACE_OUTER_BOUND('',#1489,.T.);
#1064=FACE_OUTER_BOUND('',#1490,.T.);
#1065=FACE_OUTER_BOUND('',#1491,.T.);
#1066=FACE_OUTER_BOUND('',#1492,.T.);
#1067=FACE_OUTER_BOUND('',#1493,.T.);
#1068=FACE_OUTER_BOUND('',#1494,.T.);
#1069=FACE_OUTER_BOUND('',#1495,.T.);
#1070=FACE_OUTER_BOUND('',#1496,.T.);
#1071=FACE_OUTER_BOUND('',#1497,.T.);
#1480=EDGE_LOOP('',(#4785));
#1481=EDGE_LOOP('',(#4786,#4787,#4788,#4789));
#1482=EDGE_LOOP('',(#4790,#4791,#4792,#4793));
#1483=EDGE_LOOP('',(#4794,#4795,#4796,#4797));
#1484=EDGE_LOOP('',(#4798));
#1485=EDGE_LOOP('',(#4799));
#1486=EDGE_LOOP('',(#4800,#4801,#4802,#4803));
#1487=EDGE_LOOP('',(#4804,#4805,#4806,#4807));
#1488=EDGE_LOOP('',(#4808,#4809,#4810,#4811));
#1489=EDGE_LOOP('',(#4812));
#1490=EDGE_LOOP('',(#4813,#4814,#4815,#4816));
#1491=EDGE_LOOP('',(#4817,#4818,#4819,#4820));
#1492=EDGE_LOOP('',(#4821,#4822,#4823,#4824));
#1493=EDGE_LOOP('',(#4825,#4826,#4827,#4828));
#1494=EDGE_LOOP('',(#4829,#4830,#4831,#4832));
#1495=EDGE_LOOP('',(#4833,#4834,#4835,#4836));
#1496=EDGE_LOOP('',(#4837,#4838,#4839,#4840,#4841,#4842));
#1497=EDGE_LOOP('',(#4843,#4844,#4845,#4846,#4847,#4848));
#1794=LINE('',#10288,#2104);
#1795=LINE('',#10292,#2105);
#1796=LINE('',#10296,#2106);
#1797=LINE('',#10303,#2107);
#1798=LINE('',#10307,#2108);
#1799=LINE('',#10311,#2109);
#1800=LINE('',#10316,#2110);
#1801=LINE('',#10318,#2111);
#1802=LINE('',#10320,#2112);
#1803=LINE('',#10321,#2113);
#1804=LINE('',#10324,#2114);
#1805=LINE('',#10326,#2115);
#1806=LINE('',#10327,#2116);
#1807=LINE('',#10330,#2117);
#1808=LINE('',#10332,#2118);
#1809=LINE('',#10333,#2119);
#1810=LINE('',#10336,#2120);
#1811=LINE('',#10338,#2121);
#1812=LINE('',#10339,#2122);
#1813=LINE('',#10342,#2123);
#1814=LINE('',#10344,#2124);
#1815=LINE('',#10345,#2125);
#1816=LINE('',#10347,#2126);
#1817=LINE('',#10348,#2127);
#2104=VECTOR('',#7968,0.325);
#2105=VECTOR('',#7973,0.35);
#2106=VECTOR('',#7978,0.335);
#2107=VECTOR('',#7987,0.21);
#2108=VECTOR('',#7992,0.2);
#2109=VECTOR('',#7997,0.18);
#2110=VECTOR('',#8002,1.);
#2111=VECTOR('',#8003,1.);
#2112=VECTOR('',#8004,1.);
#2113=VECTOR('',#8005,1.);
#2114=VECTOR('',#8008,1.);
#2115=VECTOR('',#8009,1.);
#2116=VECTOR('',#8010,1.);
#2117=VECTOR('',#8013,1.);
#2118=VECTOR('',#8014,1.);
#2119=VECTOR('',#8015,1.);
#2120=VECTOR('',#8018,1.);
#2121=VECTOR('',#8019,1.);
#2122=VECTOR('',#8020,1.);
#2123=VECTOR('',#8023,1.);
#2124=VECTOR('',#8024,1.);
#2125=VECTOR('',#8025,1.);
#2126=VECTOR('',#8028,1.);
#2127=VECTOR('',#8029,1.);
#2426=CIRCLE('',#6328,0.3);
#2427=CIRCLE('',#6330,0.35);
#2428=CIRCLE('',#6332,0.35);
#2429=CIRCLE('',#6334,0.32);
#2430=CIRCLE('',#6336,0.22);
#2431=CIRCLE('',#6338,0.1954);
#2432=CIRCLE('',#6340,0.1954);
#2433=CIRCLE('',#6342,0.16);
#2866=VERTEX_POINT('',#10283);
#2867=VERTEX_POINT('',#10286);
#2868=VERTEX_POINT('',#10290);
#2869=VERTEX_POINT('',#10294);
#2870=VERTEX_POINT('',#10298);
#2871=VERTEX_POINT('',#10301);
#2872=VERTEX_POINT('',#10305);
#2873=VERTEX_POINT('',#10309);
#2874=VERTEX_POINT('',#10314);
#2875=VERTEX_POINT('',#10315);
#2876=VERTEX_POINT('',#10317);
#2877=VERTEX_POINT('',#10319);
#2878=VERTEX_POINT('',#10323);
#2879=VERTEX_POINT('',#10325);
#2880=VERTEX_POINT('',#10329);
#2881=VERTEX_POINT('',#10331);
#2882=VERTEX_POINT('',#10335);
#2883=VERTEX_POINT('',#10337);
#2884=VERTEX_POINT('',#10341);
#2885=VERTEX_POINT('',#10343);
#3510=EDGE_CURVE('',#2866,#2866,#2426,.T.);
#3511=EDGE_CURVE('',#2867,#2867,#2427,.T.);
#3512=EDGE_CURVE('',#2867,#2866,#1794,.T.);
#3513=EDGE_CURVE('',#2868,#2868,#2428,.T.);
#3514=EDGE_CURVE('',#2868,#2867,#1795,.T.);
#3515=EDGE_CURVE('',#2869,#2869,#2429,.T.);
#3516=EDGE_CURVE('',#2869,#2868,#1796,.T.);
#3517=EDGE_CURVE('',#2870,#2870,#2430,.T.);
#3518=EDGE_CURVE('',#2871,#2871,#2431,.F.);
#3519=EDGE_CURVE('',#2871,#2870,#1797,.T.);
#3520=EDGE_CURVE('',#2872,#2872,#2432,.F.);
#3521=EDGE_CURVE('',#2872,#2871,#1798,.T.);
#3522=EDGE_CURVE('',#2873,#2873,#2433,.T.);
#3523=EDGE_CURVE('',#2873,#2872,#1799,.T.);
#3524=EDGE_CURVE('',#2874,#2875,#1800,.T.);
#3525=EDGE_CURVE('',#2875,#2876,#1801,.T.);
#3526=EDGE_CURVE('',#2876,#2877,#1802,.T.);
#3527=EDGE_CURVE('',#2874,#2877,#1803,.T.);
#3528=EDGE_CURVE('',#2875,#2878,#1804,.T.);
#3529=EDGE_CURVE('',#2878,#2879,#1805,.T.);
#3530=EDGE_CURVE('',#2879,#2876,#1806,.T.);
#3531=EDGE_CURVE('',#2878,#2880,#1807,.T.);
#3532=EDGE_CURVE('',#2880,#2881,#1808,.T.);
#3533=EDGE_CURVE('',#2881,#2879,#1809,.T.);
#3534=EDGE_CURVE('',#2880,#2882,#1810,.T.);
#3535=EDGE_CURVE('',#2882,#2883,#1811,.T.);
#3536=EDGE_CURVE('',#2883,#2881,#1812,.T.);
#3537=EDGE_CURVE('',#2882,#2884,#1813,.T.);
#3538=EDGE_CURVE('',#2884,#2885,#1814,.T.);
#3539=EDGE_CURVE('',#2885,#2883,#1815,.T.);
#3540=EDGE_CURVE('',#2884,#2874,#1816,.T.);
#3541=EDGE_CURVE('',#2877,#2885,#1817,.T.);
#4785=ORIENTED_EDGE('',*,*,#3510,.F.);
#4786=ORIENTED_EDGE('',*,*,#3511,.F.);
#4787=ORIENTED_EDGE('',*,*,#3512,.T.);
#4788=ORIENTED_EDGE('',*,*,#3510,.T.);
#4789=ORIENTED_EDGE('',*,*,#3512,.F.);
#4790=ORIENTED_EDGE('',*,*,#3513,.F.);
#4791=ORIENTED_EDGE('',*,*,#3514,.T.);
#4792=ORIENTED_EDGE('',*,*,#3511,.T.);
#4793=ORIENTED_EDGE('',*,*,#3514,.F.);
#4794=ORIENTED_EDGE('',*,*,#3515,.F.);
#4795=ORIENTED_EDGE('',*,*,#3516,.T.);
#4796=ORIENTED_EDGE('',*,*,#3513,.T.);
#4797=ORIENTED_EDGE('',*,*,#3516,.F.);
#4798=ORIENTED_EDGE('',*,*,#3515,.T.);
#4799=ORIENTED_EDGE('',*,*,#3517,.F.);
#4800=ORIENTED_EDGE('',*,*,#3518,.F.);
#4801=ORIENTED_EDGE('',*,*,#3519,.T.);
#4802=ORIENTED_EDGE('',*,*,#3517,.T.);
#4803=ORIENTED_EDGE('',*,*,#3519,.F.);
#4804=ORIENTED_EDGE('',*,*,#3520,.F.);
#4805=ORIENTED_EDGE('',*,*,#3521,.T.);
#4806=ORIENTED_EDGE('',*,*,#3518,.T.);
#4807=ORIENTED_EDGE('',*,*,#3521,.F.);
#4808=ORIENTED_EDGE('',*,*,#3522,.F.);
#4809=ORIENTED_EDGE('',*,*,#3523,.T.);
#4810=ORIENTED_EDGE('',*,*,#3520,.T.);
#4811=ORIENTED_EDGE('',*,*,#3523,.F.);
#4812=ORIENTED_EDGE('',*,*,#3522,.T.);
#4813=ORIENTED_EDGE('',*,*,#3524,.T.);
#4814=ORIENTED_EDGE('',*,*,#3525,.T.);
#4815=ORIENTED_EDGE('',*,*,#3526,.T.);
#4816=ORIENTED_EDGE('',*,*,#3527,.F.);
#4817=ORIENTED_EDGE('',*,*,#3528,.T.);
#4818=ORIENTED_EDGE('',*,*,#3529,.T.);
#4819=ORIENTED_EDGE('',*,*,#3530,.T.);
#4820=ORIENTED_EDGE('',*,*,#3525,.F.);
#4821=ORIENTED_EDGE('',*,*,#3531,.T.);
#4822=ORIENTED_EDGE('',*,*,#3532,.T.);
#4823=ORIENTED_EDGE('',*,*,#3533,.T.);
#4824=ORIENTED_EDGE('',*,*,#3529,.F.);
#4825=ORIENTED_EDGE('',*,*,#3534,.T.);
#4826=ORIENTED_EDGE('',*,*,#3535,.T.);
#4827=ORIENTED_EDGE('',*,*,#3536,.T.);
#4828=ORIENTED_EDGE('',*,*,#3532,.F.);
#4829=ORIENTED_EDGE('',*,*,#3537,.T.);
#4830=ORIENTED_EDGE('',*,*,#3538,.T.);
#4831=ORIENTED_EDGE('',*,*,#3539,.T.);
#4832=ORIENTED_EDGE('',*,*,#3535,.F.);
#4833=ORIENTED_EDGE('',*,*,#3540,.T.);
#4834=ORIENTED_EDGE('',*,*,#3527,.T.);
#4835=ORIENTED_EDGE('',*,*,#3541,.T.);
#4836=ORIENTED_EDGE('',*,*,#3538,.F.);
#4837=ORIENTED_EDGE('',*,*,#3540,.F.);
#4838=ORIENTED_EDGE('',*,*,#3537,.F.);
#4839=ORIENTED_EDGE('',*,*,#3534,.F.);
#4840=ORIENTED_EDGE('',*,*,#3531,.F.);
#4841=ORIENTED_EDGE('',*,*,#3528,.F.);
#4842=ORIENTED_EDGE('',*,*,#3524,.F.);
#4843=ORIENTED_EDGE('',*,*,#3541,.F.);
#4844=ORIENTED_EDGE('',*,*,#3526,.F.);
#4845=ORIENTED_EDGE('',*,*,#3530,.F.);
#4846=ORIENTED_EDGE('',*,*,#3533,.F.);
#4847=ORIENTED_EDGE('',*,*,#3536,.F.);
#4848=ORIENTED_EDGE('',*,*,#3539,.F.);
#4968=CYLINDRICAL_SURFACE('',#6331,0.35);
#4969=CYLINDRICAL_SURFACE('',#6339,0.1954);
#5267=ADVANCED_FACE('',(#1055),#747,.T.);
#5268=ADVANCED_FACE('',(#1056),#321,.T.);
#5269=ADVANCED_FACE('',(#1057),#4968,.T.);
#5270=ADVANCED_FACE('',(#1058),#322,.T.);
#5271=ADVANCED_FACE('',(#1059,#592),#748,.T.);
#5272=ADVANCED_FACE('',(#1060),#323,.T.);
#5273=ADVANCED_FACE('',(#1061),#4969,.T.);
#5274=ADVANCED_FACE('',(#1062),#324,.T.);
#5275=ADVANCED_FACE('',(#1063),#749,.T.);
#5276=ADVANCED_FACE('',(#1064),#750,.F.);
#5277=ADVANCED_FACE('',(#1065),#751,.F.);
#5278=ADVANCED_FACE('',(#1066),#752,.F.);
#5279=ADVANCED_FACE('',(#1067),#753,.F.);
#5280=ADVANCED_FACE('',(#1068),#754,.F.);
#5281=ADVANCED_FACE('',(#1069),#755,.F.);
#5282=ADVANCED_FACE('',(#1070),#756,.F.);
#5283=ADVANCED_FACE('',(#1071),#757,.F.);
#5340=CLOSED_SHELL('',(#5267,#5268,#5269,#5270,#5271,#5272,#5273,#5274,
#5275));
#5341=CLOSED_SHELL('',(#5276,#5277,#5278,#5279,#5280,#5281,#5282,#5283));
#6326=AXIS2_PLACEMENT_3D('',#10281,#7958,#7959);
#6327=AXIS2_PLACEMENT_3D('',#10282,#7960,#7961);
#6328=AXIS2_PLACEMENT_3D('',#10284,#7962,#7963);
#6329=AXIS2_PLACEMENT_3D('',#10285,#7964,#7965);
#6330=AXIS2_PLACEMENT_3D('',#10287,#7966,#7967);
#6331=AXIS2_PLACEMENT_3D('',#10289,#7969,#7970);
#6332=AXIS2_PLACEMENT_3D('',#10291,#7971,#7972);
#6333=AXIS2_PLACEMENT_3D('',#10293,#7974,#7975);
#6334=AXIS2_PLACEMENT_3D('',#10295,#7976,#7977);
#6335=AXIS2_PLACEMENT_3D('',#10297,#7979,#7980);
#6336=AXIS2_PLACEMENT_3D('',#10299,#7981,#7982);
#6337=AXIS2_PLACEMENT_3D('',#10300,#7983,#7984);
#6338=AXIS2_PLACEMENT_3D('',#10302,#7985,#7986);
#6339=AXIS2_PLACEMENT_3D('',#10304,#7988,#7989);
#6340=AXIS2_PLACEMENT_3D('',#10306,#7990,#7991);
#6341=AXIS2_PLACEMENT_3D('',#10308,#7993,#7994);
#6342=AXIS2_PLACEMENT_3D('',#10310,#7995,#7996);
#6343=AXIS2_PLACEMENT_3D('',#10312,#7998,#7999);
#6344=AXIS2_PLACEMENT_3D('',#10313,#8000,#8001);
#6345=AXIS2_PLACEMENT_3D('',#10322,#8006,#8007);
#6346=AXIS2_PLACEMENT_3D('',#10328,#8011,#8012);
#6347=AXIS2_PLACEMENT_3D('',#10334,#8016,#8017);
#6348=AXIS2_PLACEMENT_3D('',#10340,#8021,#8022);
#6349=AXIS2_PLACEMENT_3D('',#10346,#8026,#8027);
#6350=AXIS2_PLACEMENT_3D('',#10349,#8030,#8031);
#6351=AXIS2_PLACEMENT_3D('',#10350,#8032,#8033);
#7958=DIRECTION('axis',(0.,0.,1.));
#7959=DIRECTION('refdir',(1.,0.,0.));
#7960=DIRECTION('center_axis',(0.,1.,0.));
#7961=DIRECTION('ref_axis',(0.,0.,1.));
#7962=DIRECTION('center_axis',(0.,-1.,0.));
#7963=DIRECTION('ref_axis',(1.,0.,0.));
#7964=DIRECTION('center_axis',(0.,-1.,0.));
#7965=DIRECTION('ref_axis',(1.,0.,0.));
#7966=DIRECTION('center_axis',(0.,-1.,0.));
#7967=DIRECTION('ref_axis',(1.,0.,0.));
#7968=DIRECTION('',(0.707106781186547,0.707106781186548,8.65956056235493E-17));
#7969=DIRECTION('center_axis',(0.,-1.,0.));
#7970=DIRECTION('ref_axis',(1.,0.,0.));
#7971=DIRECTION('center_axis',(0.,-1.,0.));
#7972=DIRECTION('ref_axis',(1.,0.,0.));
#7973=DIRECTION('',(0.,1.,0.));
#7974=DIRECTION('center_axis',(0.,1.,0.));
#7975=DIRECTION('ref_axis',(1.,0.,0.));
#7976=DIRECTION('center_axis',(0.,-1.,0.));
#7977=DIRECTION('ref_axis',(1.,0.,0.));
#7978=DIRECTION('',(-0.707106781186547,0.707106781186548,-8.65956056235493E-17));
#7979=DIRECTION('center_axis',(0.,-1.,0.));
#7980=DIRECTION('ref_axis',(0.,0.,-1.));
#7981=DIRECTION('center_axis',(0.,-1.,0.));
#7982=DIRECTION('ref_axis',(1.,0.,0.));
#7983=DIRECTION('center_axis',(0.,1.,0.));
#7984=DIRECTION('ref_axis',(1.,0.,0.));
#7985=DIRECTION('center_axis',(0.,1.,0.));
#7986=DIRECTION('ref_axis',(1.,0.,0.));
#7987=DIRECTION('',(-0.447213595499958,0.894427190999916,-5.47678698264203E-17));
#7988=DIRECTION('center_axis',(0.,-1.,0.));
#7989=DIRECTION('ref_axis',(1.,0.,0.));
#7990=DIRECTION('center_axis',(0.,1.,0.));
#7991=DIRECTION('ref_axis',(1.,0.,0.));
#7992=DIRECTION('',(0.,1.,0.));
#7993=DIRECTION('center_axis',(0.,1.,0.));
#7994=DIRECTION('ref_axis',(1.,0.,0.));
#7995=DIRECTION('center_axis',(0.,-1.,0.));
#7996=DIRECTION('ref_axis',(1.,0.,0.));
#7997=DIRECTION('',(-0.707106781186547,0.707106781186548,-8.65956056235493E-17));
#7998=DIRECTION('center_axis',(0.,-1.,0.));
#7999=DIRECTION('ref_axis',(0.,0.,-1.));
#8000=DIRECTION('center_axis',(0.866025403784439,0.,-0.5));
#8001=DIRECTION('ref_axis',(0.5,0.,0.866025403784439));
#8002=DIRECTION('',(-0.5,0.,-0.866025403784439));
#8003=DIRECTION('',(0.,-1.,0.));
#8004=DIRECTION('',(0.5,0.,0.866025403784439));
#8005=DIRECTION('',(0.,-1.,0.));
#8006=DIRECTION('center_axis',(1.60246890531964E-16,0.,-1.));
#8007=DIRECTION('ref_axis',(1.,0.,1.60246890531964E-16));
#8008=DIRECTION('',(-1.,0.,-1.60246890531964E-16));
#8009=DIRECTION('',(0.,-1.,0.));
#8010=DIRECTION('',(1.,0.,1.60246890531964E-16));
#8011=DIRECTION('center_axis',(-0.866025403784439,0.,-0.5));
#8012=DIRECTION('ref_axis',(0.5,0.,-0.866025403784439));
#8013=DIRECTION('',(-0.5,0.,0.866025403784439));
#8014=DIRECTION('',(0.,-1.,0.));
#8015=DIRECTION('',(0.5,0.,-0.866025403784439));
#8016=DIRECTION('center_axis',(-0.866025403784439,0.,0.5));
#8017=DIRECTION('ref_axis',(-0.5,0.,-0.866025403784439));
#8018=DIRECTION('',(0.5,0.,0.866025403784439));
#8019=DIRECTION('',(0.,-1.,0.));
#8020=DIRECTION('',(-0.5,0.,-0.866025403784439));
#8021=DIRECTION('center_axis',(-1.60246890531964E-16,0.,1.));
#8022=DIRECTION('ref_axis',(-1.,0.,-1.60246890531964E-16));
#8023=DIRECTION('',(1.,0.,1.60246890531964E-16));
#8024=DIRECTION('',(0.,-1.,0.));
#8025=DIRECTION('',(-1.,0.,-1.60246890531964E-16));
#8026=DIRECTION('center_axis',(0.866025403784439,0.,0.5));
#8027=DIRECTION('ref_axis',(-0.5,0.,0.866025403784439));
#8028=DIRECTION('',(0.5,0.,-0.866025403784439));
#8029=DIRECTION('',(-0.5,0.,0.866025403784439));
#8030=DIRECTION('center_axis',(0.,1.,0.));
#8031=DIRECTION('ref_axis',(1.,0.,0.));
#8032=DIRECTION('center_axis',(0.,-1.,0.));
#8033=DIRECTION('ref_axis',(0.,0.,-1.));
#10281=CARTESIAN_POINT('',(0.,0.,0.));
#10282=CARTESIAN_POINT('Origin',(0.3,0.4,0.));
#10283=CARTESIAN_POINT('',(-0.3,0.4,-3.67394039744206E-17));
#10284=CARTESIAN_POINT('Origin',(0.,0.4,0.));
#10285=CARTESIAN_POINT('Origin',(0.,0.375,0.));
#10286=CARTESIAN_POINT('',(-0.35,0.35,-4.28626379701573E-17));
#10287=CARTESIAN_POINT('Origin',(0.,0.35,0.));
#10288=CARTESIAN_POINT('',(-0.325,0.375,-3.9801020972289E-17));
#10289=CARTESIAN_POINT('Origin',(0.,0.19,0.));
#10290=CARTESIAN_POINT('',(-0.35,0.03,-4.28626379701574E-17));
#10291=CARTESIAN_POINT('Origin',(0.,0.03,0.));
#10292=CARTESIAN_POINT('',(-0.35,0.19,-4.28626379701574E-17));
#10293=CARTESIAN_POINT('Origin',(0.,0.0149999999999999,0.));
#10294=CARTESIAN_POINT('',(-0.32,-3.29597460435593E-17,-3.91886975727153E-17));
#10295=CARTESIAN_POINT('Origin',(0.,0.,0.));
#10296=CARTESIAN_POINT('',(-0.335,0.0149999999999999,-4.10256677714363E-17));
#10297=CARTESIAN_POINT('Origin',(0.22,0.,0.));
#10298=CARTESIAN_POINT('',(-0.22,-6.93889390390723E-18,-2.69422295812418E-17));
#10299=CARTESIAN_POINT('Origin',(0.,0.,0.));
#10300=CARTESIAN_POINT('Origin',(0.,-0.02,0.));
#10301=CARTESIAN_POINT('',(-0.1954,-0.0492,2.39295984553393E-17));
#10302=CARTESIAN_POINT('Origin',(0.,-0.0492,0.));
#10303=CARTESIAN_POINT('',(-0.21,-0.02,-2.57175827820944E-17));
#10304=CARTESIAN_POINT('Origin',(0.,-0.8,0.));
#10305=CARTESIAN_POINT('',(-0.1954,-1.5646,2.39295984553393E-17));
#10306=CARTESIAN_POINT('Origin',(0.,-1.5646,0.));
#10307=CARTESIAN_POINT('',(-0.1954,-0.8,-2.39295984553393E-17));
#10308=CARTESIAN_POINT('Origin',(0.,-1.58,0.));
#10309=CARTESIAN_POINT('',(-0.16,-1.6,-1.95943487863577E-17));
#10310=CARTESIAN_POINT('Origin',(0.,-1.6,0.));
#10311=CARTESIAN_POINT('',(-0.18,-1.58,-2.20436423846524E-17));
#10312=CARTESIAN_POINT('Origin',(0.,-1.6,0.));
#10313=CARTESIAN_POINT('Origin',(0.0866025403784439,-0.4,-0.15));
#10314=CARTESIAN_POINT('',(0.173205080756888,-0.4,0.));
#10315=CARTESIAN_POINT('',(0.0866025403784439,-0.4,-0.15));
#10316=CARTESIAN_POINT('',(0.173205080756888,-0.4,0.));
#10317=CARTESIAN_POINT('',(0.0866025403784439,-0.64,-0.15));
#10318=CARTESIAN_POINT('',(0.0866025403784439,-0.4,-0.15));
#10319=CARTESIAN_POINT('',(0.173205080756888,-0.64,0.));
#10320=CARTESIAN_POINT('',(0.173205080756888,-0.64,0.));
#10321=CARTESIAN_POINT('',(0.173205080756888,-0.4,0.));
#10322=CARTESIAN_POINT('Origin',(-0.0866025403784438,-0.4,-0.15));
#10323=CARTESIAN_POINT('',(-0.0866025403784438,-0.4,-0.15));
#10324=CARTESIAN_POINT('',(0.0866025403784439,-0.4,-0.15));
#10325=CARTESIAN_POINT('',(-0.0866025403784438,-0.64,-0.15));
#10326=CARTESIAN_POINT('',(-0.0866025403784438,-0.4,-0.15));
#10327=CARTESIAN_POINT('',(0.0866025403784439,-0.64,-0.15));
#10328=CARTESIAN_POINT('Origin',(-0.173205080756888,-0.4,-2.77555756156289E-17));
#10329=CARTESIAN_POINT('',(-0.173205080756888,-0.4,-2.12115047744981E-17));
#10330=CARTESIAN_POINT('',(-0.0866025403784438,-0.4,-0.15));
#10331=CARTESIAN_POINT('',(-0.173205080756888,-0.64,-2.77555756156289E-17));
#10332=CARTESIAN_POINT('',(-0.173205080756888,-0.4,-2.12115047744981E-17));
#10333=CARTESIAN_POINT('',(-0.0866025403784438,-0.64,-0.15));
#10334=CARTESIAN_POINT('Origin',(-0.0866025403784439,-0.4,0.15));
#10335=CARTESIAN_POINT('',(-0.0866025403784439,-0.4,0.15));
#10336=CARTESIAN_POINT('',(-0.173205080756888,-0.4,-2.12115047744981E-17));
#10337=CARTESIAN_POINT('',(-0.0866025403784439,-0.64,0.15));
#10338=CARTESIAN_POINT('',(-0.0866025403784439,-0.4,0.15));
#10339=CARTESIAN_POINT('',(-0.173205080756888,-0.64,-2.12115047744981E-17));
#10340=CARTESIAN_POINT('Origin',(0.0866025403784439,-0.4,0.15));
#10341=CARTESIAN_POINT('',(0.0866025403784439,-0.4,0.15));
#10342=CARTESIAN_POINT('',(-0.0866025403784439,-0.4,0.15));
#10343=CARTESIAN_POINT('',(0.0866025403784439,-0.64,0.15));
#10344=CARTESIAN_POINT('',(0.0866025403784439,-0.4,0.15));
#10345=CARTESIAN_POINT('',(-0.0866025403784439,-0.64,0.15));
#10346=CARTESIAN_POINT('Origin',(0.173205080756888,-0.4,0.));
#10347=CARTESIAN_POINT('',(0.0866025403784439,-0.4,0.15));
#10348=CARTESIAN_POINT('',(0.0866025403784439,-0.64,0.15));
#10349=CARTESIAN_POINT('Origin',(0.,-0.4,-2.77555756156289E-17));
#10350=CARTESIAN_POINT('Origin',(0.,-0.64,-2.77555756156289E-17));
#10467=UNCERTAINTY_MEASURE_WITH_UNIT(LENGTH_MEASURE(0.001),#10511,
'DISTANCE_ACCURACY_VALUE',
'Maximum model space distance between geometric entities at asserted c
onnectivities');
#10471=UNCERTAINTY_MEASURE_WITH_UNIT(LENGTH_MEASURE(0.001),#10511,
'DISTANCE_ACCURACY_VALUE',
'Maximum model space distance between geometric entities at asserted c
onnectivities');
#10506=(
GEOMETRIC_REPRESENTATION_CONTEXT(3)
GLOBAL_UNCERTAINTY_ASSIGNED_CONTEXT((#10467))
GLOBAL_UNIT_ASSIGNED_CONTEXT((#10511,#10513,#10514))
REPRESENTATION_CONTEXT('','3D')
);
#10510=(
GEOMETRIC_REPRESENTATION_CONTEXT(3)
GLOBAL_UNCERTAINTY_ASSIGNED_CONTEXT((#10471))
GLOBAL_UNIT_ASSIGNED_CONTEXT((#10511,#10513,#10514))
REPRESENTATION_CONTEXT('','3D')
);
#10511=(
LENGTH_UNIT()
NAMED_UNIT(*)
SI_UNIT(.CENTI.,.METRE.)
);
#10513=(
NAMED_UNIT(*)
PLANE_ANGLE_UNIT()
SI_UNIT($,.RADIAN.)
);
#10514=(
NAMED_UNIT(*)
SI_UNIT($,.STERADIAN.)
SOLID_ANGLE_UNIT()
);
#10549=SHAPE_DEFINITION_REPRESENTATION(#10597,#10679);
#10597=PRODUCT_DEFINITION_SHAPE('',$,#10718);
#10679=SHAPE_REPRESENTATION('',(#6326),#10506);
#10683=PRODUCT_DEFINITION_CONTEXT('part definition',#10799,'design');
#10718=PRODUCT_DEFINITION('Cap Screw - M4x16','Cap Screw - M4x16',#10756,
#10683);
#10756=PRODUCT_DEFINITION_FORMATION('',$,#10835);
#10799=APPLICATION_CONTEXT(
'Core Data for Automotive Mechanical Design Process');
#10800=PRODUCT_CONTEXT('part definition',#10799,'mechanical');
#10835=PRODUCT('Cap Screw - M4x16','Cap Screw - M4x16',
'Cap Screw - M4x16',(#10800));
#10909=COLOUR_RGB('Black',0.12,0.14,0.17);
#10910=FILL_AREA_STYLE_COLOUR('',#10909);
#10911=FILL_AREA_STYLE('',(#10910));
#10912=SURFACE_STYLE_FILL_AREA(#10911);
#10913=SURFACE_SIDE_STYLE('',(#10912));
#10914=SURFACE_STYLE_USAGE(.BOTH.,#10913);
#10915=PRESENTATION_STYLE_ASSIGNMENT((#10914));
ENDSEC;
END-ISO-10303-21;
